ISO-10303-21;
HEADER;
FILE_DESCRIPTION (('STEP AP214'),
    '1' );
FILE_NAME ('O Ring Seal 3.step',
    '2026-10-05T22:38:29',
    ( '' ),
    ( '' ),
    'SwSTEP 2.0',
    'SolidWorks 2020',
    '' );
FILE_SCHEMA (( 'AUTOMOTIVE_DESIGN' ));
ENDSEC;

DATA;
#466=EDGE_CURVE ( 'NONE', #45574, #28824, #50443, .T. ) ;
#806=( GEOMETRIC_REPRESENTATION_CONTEXT ( 3 ) GLOBAL_UNCERTAINTY_ASSIGNED_CONTEXT ( ( #18298 ) ) GLOBAL_UNIT_ASSIGNED_CONTEXT ( ( #13706, #60212, #45521 ) ) REPRESENTATION_CONTEXT ( 'NONE', 'WORKASPACE' ) );
#842=DIRECTION ( 'NONE',  ( 1.000000000000000000, 0.000000000000000000, 0.000000000000000000 ) ) ;
#850=CYLINDRICAL_SURFACE ( 'NONE', #44076, 11.84999999999999964 ) ;
#1486=ADVANCED_FACE ( 'NONE', ( #33394 ), #6869, .T. ) ;
#1921=COLOUR_RGB ( '', 0.08235294, 0.09019608, 0.10196078) ;
#2431=CARTESIAN_POINT ( 'NONE',  ( 8.099999999999999645, 0.000000000000000000, 0.000000000000000000 ) ) ;
#3049=COLOUR_RGB ( '', 0.08235294, 0.09019608, 0.10196078) ;
#3204=SHAPE_REPRESENTATION_RELATIONSHIP ( 'NONE' , 'NONE' ,  #12958, #43565 ) ;
#3615=VECTOR ( 'NONE', #842, 1000.000000000000000 ) ;
#3934=EDGE_CURVE ( 'NONE', #66816, #59953, #13552, .T. ) ;
#4135=CARTESIAN_POINT ( 'NONE',  ( 8.099999999999999645, 0.000000000000000000, 0.000000000000000000 ) ) ;
#4139=STYLED_ITEM ( 'NONE', ( #51441 ), #43565 ) ;
#4985=CARTESIAN_POINT ( 'NONE',  ( 7.100000000000000533, 0.000000000000000000, 0.000000000000000000 ) ) ;
#5176=DIRECTION ( 'NONE',  ( 1.000000000000000000, 0.000000000000000000, 0.000000000000000000 ) ) ;
#5281=DIRECTION ( 'NONE',  ( 0.000000000000000000, -1.000000000000000000, 0.000000000000000000 ) ) ;
#5447=SURFACE_SIDE_STYLE ('',( #37601 ) ) ;
#5674=ADVANCED_FACE ( 'NONE', ( #50133 ), #850, .F. ) ;
#5694=AXIS2_PLACEMENT_3D ( 'NONE', #2431, #67086, #40520 ) ;
#6342=EDGE_LOOP ( 'NONE', ( #38603, #35784 ) ) ;
#6659=CARTESIAN_POINT ( 'NONE',  ( 7.100000000000000533, 0.000000000000000000, 0.000000000000000000 ) ) ;
#6869=TOROIDAL_SURFACE ( 'NONE', #11357, 12.35000000006999876, 0.5000000000000000000 ) ;
#7377=CARTESIAN_POINT ( 'NONE',  ( 7.600000000000000533, -12.34999999999999964, -4.046978686977000011E-05 ) ) ;
#7468=DIRECTION ( 'NONE',  ( 0.000000000000000000, -1.000000000000000000, 0.000000000000000000 ) ) ;
#7721=CARTESIAN_POINT ( 'NONE',  ( 7.100000000000000533, -11.84999999999999964, 0.000000000000000000 ) ) ;
#7974=CARTESIAN_POINT ( 'NONE',  ( 7.600000000000000533, 12.34999999999999964, 4.046978687741000012E-05 ) ) ;
#8306=DIRECTION ( 'NONE',  ( -1.000000000000000000, 0.000000000000000000, 0.000000000000000000 ) ) ;
#8314=DIRECTION ( 'NONE',  ( 0.9999999999938153916, -3.516990153967782703E-06, -1.152484550329262306E-11 ) ) ;
#9676=AXIS2_PLACEMENT_3D ( 'NONE', #40345, #19020, #18341 ) ;
#9726=CARTESIAN_POINT ( 'NONE',  ( 7.100000000000000533, 11.84999999999999964, 0.000000000000000000 ) ) ;
#9912=AXIS2_PLACEMENT_3D ( 'NONE', #4135, #62526, #41894 ) ;
#9950=EDGE_LOOP ( 'NONE', ( #35019, #24666 ) ) ;
#10260=AXIS2_PLACEMENT_3D ( 'NONE', #23317, #45681, #24006 ) ;
#10344=FILL_AREA_STYLE_COLOUR ( '', #1921 ) ;
#10684=( NAMED_UNIT ( * ) PLANE_ANGLE_UNIT ( ) SI_UNIT ( $, .RADIAN. ) );
#10837=( GEOMETRIC_REPRESENTATION_CONTEXT ( 3 ) GLOBAL_UNCERTAINTY_ASSIGNED_CONTEXT ( ( #42289 ) ) GLOBAL_UNIT_ASSIGNED_CONTEXT ( ( #24874, #46887, #45858 ) ) REPRESENTATION_CONTEXT ( 'NONE', 'WORKASPACE' ) );
#10957=EDGE_CURVE ( 'NONE', #59953, #66816, #65983, .T. ) ;
#11042=EDGE_CURVE ( 'NONE', #28824, #45574, #35569, .T. ) ;
#11090=ADVANCED_FACE ( 'NONE', ( #63557, #69151 ), #48174, .T. ) ;
#11176=VERTEX_POINT ( 'NONE', #9726 ) ;
#11341=CIRCLE ( 'NONE', #67033, 0.4999999999999997224 ) ;
#11357=AXIS2_PLACEMENT_3D ( 'NONE', #49458, #54358, #12063 ) ;
#12063=DIRECTION ( 'NONE',  ( 0.000000000000000000, -0.9999808993455937545, -0.006180691221632959691 ) ) ;
#12176=ORIENTED_EDGE ( 'NONE', *, *, #23041, .T. ) ;
#12359=APPLICATION_CONTEXT ( 'automotive_design' ) ;
#12390=AXIS2_PLACEMENT_3D ( 'NONE', #21027, #8306, #13220 ) ;
#12958=SHAPE_REPRESENTATION ( 'O Ring Seal 3', ( #9676 ), #806 ) ;
#13220=DIRECTION ( 'NONE',  ( 0.000000000000000000, -1.000000000000000000, 0.000000000000000000 ) ) ;
#13413=EDGE_CURVE ( 'NONE', #16052, #18161, #15454, .T. ) ;
#13552=CIRCLE ( 'NONE', #12390, 11.84999999999999964 ) ;
#13706=( LENGTH_UNIT ( ) NAMED_UNIT ( * ) SI_UNIT ( .MILLI., .METRE. ) );
#13747=PRODUCT ( 'O Ring Seal 3', 'O Ring Seal 3', '', ( #40742 ) ) ;
#13836=CARTESIAN_POINT ( 'NONE',  ( 7.100000000000000533, -12.35000000006999876, 0.000000000000000000 ) ) ;
#14098=CARTESIAN_POINT ( 'NONE',  ( 8.099999999999999645, 12.35000000006999876, 0.000000000000000000 ) ) ;
#14245=( GEOMETRIC_REPRESENTATION_CONTEXT ( 3 ) GLOBAL_UNCERTAINTY_ASSIGNED_CONTEXT ( ( #36694 ) ) GLOBAL_UNIT_ASSIGNED_CONTEXT ( ( #64163, #10684, #48098 ) ) REPRESENTATION_CONTEXT ( 'NONE', 'WORKASPACE' ) );
#14253=AXIS2_PLACEMENT_3D ( 'NONE', #6659, #17505, #5281 ) ;
#14339=ORIENTED_EDGE ( 'NONE', *, *, #36484, .F. ) ;
#15454=CIRCLE ( 'NONE', #57870, 12.35000000006999876 ) ;
#15486=DIRECTION ( 'NONE',  ( 0.000000000000000000, -1.000000000000000000, 0.000000000000000000 ) ) ;
#15492=CARTESIAN_POINT ( 'NONE',  ( 8.099999999999999645, 11.84999999999999964, 0.000000000000000000 ) ) ;
#15637=DIRECTION ( 'NONE',  ( -1.000000000000000000, 0.000000000000000000, 0.000000000000000000 ) ) ;
#16052=VERTEX_POINT ( 'NONE', #13836 ) ;
#17306=ORIENTED_EDGE ( 'NONE', *, *, #17404, .T. ) ;
#17404=EDGE_CURVE ( 'NONE', #55971, #66816, #30198, .T. ) ;
#17505=DIRECTION ( 'NONE',  ( -1.000000000000000000, 0.000000000000000000, 0.000000000000000000 ) ) ;
#17913=SURFACE_STYLE_FILL_AREA ( #65788 ) ;
#18161=VERTEX_POINT ( 'NONE', #40848 ) ;
#18298=UNCERTAINTY_MEASURE_WITH_UNIT (LENGTH_MEASURE( 1.000000000000000082E-05 ), #13706, 'distance_accuracy_value', 'NONE');
#18341=DIRECTION ( 'NONE',  ( 1.000000000000000000, 0.000000000000000000, 0.000000000000000000 ) ) ;
#18569=DIRECTION ( 'NONE',  ( -2.154007395656495261E-21, 3.276905819395100166E-06, -0.9999999999946310725 ) ) ;
#19020=DIRECTION ( 'NONE',  ( 0.000000000000000000, 0.000000000000000000, 1.000000000000000000 ) ) ;
#19292=DIRECTION ( 'NONE',  ( 1.000000000000000000, 0.000000000000000000, 0.000000000000000000 ) ) ;
#19781=STYLED_ITEM ( 'NONE', ( #26086 ), #50398 ) ;
#19792=ORIENTED_EDGE ( 'NONE', *, *, #31447, .T. ) ;
#19973=EDGE_CURVE ( 'NONE', #45574, #16052, #11341, .T. ) ;
#20339=EDGE_LOOP ( 'NONE', ( #29809, #14339, #40192, #24265 ) ) ;
#20791=ORIENTED_EDGE ( 'NONE', *, *, #28627, .F. ) ;
#21027=CARTESIAN_POINT ( 'NONE',  ( 8.099999999999999645, 0.000000000000000000, 0.000000000000000000 ) ) ;
#21902=DIRECTION ( 'NONE',  ( 0.000000000000000000, -1.000000000000000000, 0.000000000000000000 ) ) ;
#22333=VECTOR ( 'NONE', #62001, 1000.000000000000000 ) ;
#22457=ORIENTED_EDGE ( 'NONE', *, *, #13413, .F. ) ;
#22866=PRODUCT_DEFINITION_FORMATION_WITH_SPECIFIED_SOURCE ( 'ANY', '', #13747, .NOT_KNOWN. ) ;
#23041=EDGE_CURVE ( 'NONE', #28824, #18161, #68228, .T. ) ;
#23178=EDGE_LOOP ( 'NONE', ( #38631, #61322 ) ) ;
#23317=CARTESIAN_POINT ( 'NONE',  ( 8.099999999999999645, 0.000000000000000000, 0.000000000000000000 ) ) ;
#24006=DIRECTION ( 'NONE',  ( 0.000000000000000000, -1.000000000000000000, 0.000000000000000000 ) ) ;
#24265=ORIENTED_EDGE ( 'NONE', *, *, #11042, .T. ) ;
#24666=ORIENTED_EDGE ( 'NONE', *, *, #45423, .F. ) ;
#24769=ORIENTED_EDGE ( 'NONE', *, *, #28627, .T. ) ;
#24874=( LENGTH_UNIT ( ) NAMED_UNIT ( * ) SI_UNIT ( .MILLI., .METRE. ) );
#25225=DIRECTION ( 'NONE',  ( 0.000000000000000000, 1.000000000000000000, 0.000000000000000000 ) ) ;
#26086=PRESENTATION_STYLE_ASSIGNMENT (( #37262 ) ) ;
#26386=CARTESIAN_POINT ( 'NONE',  ( 7.100000000000000533, 11.84999999999999964, 0.000000000000000000 ) ) ;
#27421=DIRECTION ( 'NONE',  ( 1.000000000000000000, 0.000000000000000000, 0.000000000000000000 ) ) ;
#28400=ORIENTED_EDGE ( 'NONE', *, *, #3934, .F. ) ;
#28627=EDGE_CURVE ( 'NONE', #11176, #59953, #31631, .T. ) ;
#28824=VERTEX_POINT ( 'NONE', #14098 ) ;
#28890=AXIS2_PLACEMENT_3D ( 'NONE', #4985, #31567, #15486 ) ;
#29199=CLOSED_SHELL ( 'NONE', ( #1486, #60864, #11090, #5674, #47187, #33245 ) ) ;
#29809=ORIENTED_EDGE ( 'NONE', *, *, #19973, .T. ) ;
#30105=EDGE_LOOP ( 'NONE', ( #24769, #28400, #63679, #66422 ) ) ;
#30198=LINE ( 'NONE', #45243, #22333 ) ;
#31146=AXIS2_PLACEMENT_3D ( 'NONE', #42588, #5176, #53077 ) ;
#31230=FACE_OUTER_BOUND ( 'NONE', #30105, .T. ) ;
#31336=FILL_AREA_STYLE ('',( #10344 ) ) ;
#31421=AXIS2_PLACEMENT_3D ( 'NONE', #7974, #61110, #8314 ) ;
#31447=EDGE_CURVE ( 'NONE', #11176, #55971, #42847, .T. ) ;
#31567=DIRECTION ( 'NONE',  ( 1.000000000000000000, 0.000000000000000000, 0.000000000000000000 ) ) ;
#31631=LINE ( 'NONE', #26386, #3615 ) ;
#31681=DIRECTION ( 'NONE',  ( -1.000000000000000000, 0.000000000000000000, 0.000000000000000000 ) ) ;
#33245=ADVANCED_FACE ( 'NONE', ( #36060, #50774 ), #66843, .F. ) ;
#33394=FACE_OUTER_BOUND ( 'NONE', #68179, .T. ) ;
#33420=DIRECTION ( 'NONE',  ( 0.000000000000000000, 0.9999808993455937545, 0.006180691221632959691 ) ) ;
#35019=ORIENTED_EDGE ( 'NONE', *, *, #31447, .F. ) ;
#35467=CIRCLE ( 'NONE', #14253, 11.84999999999999964 ) ;
#35509=SHAPE_DEFINITION_REPRESENTATION ( #51151, #12958 ) ;
#35569=CIRCLE ( 'NONE', #9912, 12.35000000006999876 ) ;
#35784=ORIENTED_EDGE ( 'NONE', *, *, #3934, .T. ) ;
#36060=FACE_BOUND ( 'NONE', #9950, .T. ) ;
#36184=ORIENTED_EDGE ( 'NONE', *, *, #11042, .F. ) ;
#36484=EDGE_CURVE ( 'NONE', #18161, #16052, #58495, .T. ) ;
#36694=UNCERTAINTY_MEASURE_WITH_UNIT (LENGTH_MEASURE( 1.000000000000000082E-05 ), #64163, 'distance_accuracy_value', 'NONE');
#36926=DIRECTION ( 'NONE',  ( 0.000000000000000000, 1.000000000000000000, 0.000000000000000000 ) ) ;
#37151=CYLINDRICAL_SURFACE ( 'NONE', #28890, 11.84999999999999964 ) ;
#37262=SURFACE_STYLE_USAGE ( .BOTH. , #5447 ) ;
#37601=SURFACE_STYLE_FILL_AREA ( #31336 ) ;
#38090=PRODUCT_DEFINITION ( 'UNKNOWN', '', #22866, #41588 ) ;
#38414=CARTESIAN_POINT ( 'NONE',  ( 8.099999999999999645, -12.35000000006999876, 0.000000000000000000 ) ) ;
#38552=TOROIDAL_SURFACE ( 'NONE', #44115, 12.35000000006999876, 0.5000000000000000000 ) ;
#38603=ORIENTED_EDGE ( 'NONE', *, *, #10957, .T. ) ;
#38631=ORIENTED_EDGE ( 'NONE', *, *, #13413, .T. ) ;
#39608=AXIS2_PLACEMENT_3D ( 'NONE', #40966, #19292, #25225 ) ;
#40192=ORIENTED_EDGE ( 'NONE', *, *, #23041, .F. ) ;
#40345=CARTESIAN_POINT ( 'NONE',  ( 0.000000000000000000, 0.000000000000000000, 0.000000000000000000 ) ) ;
#40520=DIRECTION ( 'NONE',  ( 0.000000000000000000, 1.000000000000000000, 0.000000000000000000 ) ) ;
#40742=PRODUCT_CONTEXT ( 'NONE', #12359, 'mechanical' ) ;
#40848=CARTESIAN_POINT ( 'NONE',  ( 7.100000000000000533, 12.35000000006999876, 0.000000000000000000 ) ) ;
#40966=CARTESIAN_POINT ( 'NONE',  ( 7.100000000000000533, 0.000000000000000000, 0.000000000000000000 ) ) ;
#41588=PRODUCT_DEFINITION_CONTEXT ( 'detailed design', #45855, 'design' ) ;
#41894=DIRECTION ( 'NONE',  ( 0.000000000000000000, 1.000000000000000000, 0.000000000000000000 ) ) ;
#42289=UNCERTAINTY_MEASURE_WITH_UNIT (LENGTH_MEASURE( 1.000000000000000082E-05 ), #24874, 'distance_accuracy_value', 'NONE');
#42588=CARTESIAN_POINT ( 'NONE',  ( 8.099999999999999645, 0.000000000000000000, 0.000000000000000000 ) ) ;
#42847=CIRCLE ( 'NONE', #57359, 11.84999999999999964 ) ;
#43565=ADVANCED_BREP_SHAPE_REPRESENTATION ( '', ( #50398, #9676 ), #806 ) ;
#44076=AXIS2_PLACEMENT_3D ( 'NONE', #55373, #27421, #7468 ) ;
#44115=AXIS2_PLACEMENT_3D ( 'NONE', #65907, #59634, #33420 ) ;
#45243=CARTESIAN_POINT ( 'NONE',  ( 7.100000000000000533, -11.84999999999999964, 0.000000000000000000 ) ) ;
#45423=EDGE_CURVE ( 'NONE', #55971, #11176, #35467, .T. ) ;
#45521=( NAMED_UNIT ( * ) SI_UNIT ( $, .STERADIAN. ) SOLID_ANGLE_UNIT ( ) );
#45574=VERTEX_POINT ( 'NONE', #38414 ) ;
#45681=DIRECTION ( 'NONE',  ( -1.000000000000000000, 0.000000000000000000, 0.000000000000000000 ) ) ;
#45855=APPLICATION_CONTEXT ( 'automotive_design' ) ;
#45858=( NAMED_UNIT ( * ) SI_UNIT ( $, .STERADIAN. ) SOLID_ANGLE_UNIT ( ) );
#46758=ORIENTED_EDGE ( 'NONE', *, *, #10957, .F. ) ;
#46887=( NAMED_UNIT ( * ) PLANE_ANGLE_UNIT ( ) SI_UNIT ( $, .RADIAN. ) );
#47187=ADVANCED_FACE ( 'NONE', ( #31230 ), #37151, .F. ) ;
#48098=( NAMED_UNIT ( * ) SI_UNIT ( $, .STERADIAN. ) SOLID_ANGLE_UNIT ( ) );
#48174=PLANE ( 'NONE',  #31146 ) ;
#48251=EDGE_LOOP ( 'NONE', ( #17306, #46758, #20791, #19792 ) ) ;
#49458=CARTESIAN_POINT ( 'NONE',  ( 7.600000000000000533, 0.000000000000000000, 0.000000000000000000 ) ) ;
#50035=DIRECTION ( 'NONE',  ( 0.9999999999938153916, 3.516990153967782703E-06, 1.152484550329262306E-11 ) ) ;
#50133=FACE_OUTER_BOUND ( 'NONE', #48251, .T. ) ;
#50398=MANIFOLD_SOLID_BREP ( 'Stock-MAS-678-1', #29199 ) ;
#50443=CIRCLE ( 'NONE', #10260, 12.35000000006999876 ) ;
#50774=FACE_OUTER_BOUND ( 'NONE', #23178, .T. ) ;
#51073=MECHANICAL_DESIGN_GEOMETRIC_PRESENTATION_REPRESENTATION('',(#4139),#10837);
#51151=PRODUCT_DEFINITION_SHAPE ( 'NONE', 'NONE',  #38090 ) ;
#51441=PRESENTATION_STYLE_ASSIGNMENT (( #56695 ) ) ;
#53077=DIRECTION ( 'NONE',  ( 0.000000000000000000, 1.000000000000000000, 0.000000000000000000 ) ) ;
#53468=ORIENTED_EDGE ( 'NONE', *, *, #466, .T. ) ;
#53702=FACE_OUTER_BOUND ( 'NONE', #20339, .T. ) ;
#54358=DIRECTION ( 'NONE',  ( 1.000000000000000000, 0.000000000000000000, 0.000000000000000000 ) ) ;
#55373=CARTESIAN_POINT ( 'NONE',  ( 7.100000000000000533, 0.000000000000000000, 0.000000000000000000 ) ) ;
#55971=VERTEX_POINT ( 'NONE', #7721 ) ;
#56349=FILL_AREA_STYLE_COLOUR ( '', #3049 ) ;
#56695=SURFACE_STYLE_USAGE ( .BOTH. , #62275 ) ;
#57359=AXIS2_PLACEMENT_3D ( 'NONE', #66697, #61460, #57577 ) ;
#57577=DIRECTION ( 'NONE',  ( 0.000000000000000000, 1.000000000000000000, 0.000000000000000000 ) ) ;
#57870=AXIS2_PLACEMENT_3D ( 'NONE', #59313, #15637, #21902 ) ;
#58495=CIRCLE ( 'NONE', #59594, 12.35000000006999876 ) ;
#58585=CARTESIAN_POINT ( 'NONE',  ( 7.100000000000000533, 0.000000000000000000, 0.000000000000000000 ) ) ;
#58846=MECHANICAL_DESIGN_GEOMETRIC_PRESENTATION_REPRESENTATION('',(#19781),#14245);
#59313=CARTESIAN_POINT ( 'NONE',  ( 7.100000000000000533, 0.000000000000000000, 0.000000000000000000 ) ) ;
#59594=AXIS2_PLACEMENT_3D ( 'NONE', #58585, #31681, #36926 ) ;
#59634=DIRECTION ( 'NONE',  ( 1.000000000000000000, 0.000000000000000000, 0.000000000000000000 ) ) ;
#59953=VERTEX_POINT ( 'NONE', #15492 ) ;
#60212=( NAMED_UNIT ( * ) PLANE_ANGLE_UNIT ( ) SI_UNIT ( $, .RADIAN. ) );
#60864=ADVANCED_FACE ( 'NONE', ( #53702 ), #38552, .T. ) ;
#60964=EDGE_LOOP ( 'NONE', ( #66904, #36184 ) ) ;
#61110=DIRECTION ( 'NONE',  ( -4.331025598861020273E-21, -3.276905820014099985E-06, 0.9999999999946310725 ) ) ;
#61322=ORIENTED_EDGE ( 'NONE', *, *, #36484, .T. ) ;
#61460=DIRECTION ( 'NONE',  ( -1.000000000000000000, 0.000000000000000000, 0.000000000000000000 ) ) ;
#62001=DIRECTION ( 'NONE',  ( 1.000000000000000000, 0.000000000000000000, 0.000000000000000000 ) ) ;
#62275=SURFACE_SIDE_STYLE ('',( #17913 ) ) ;
#62526=DIRECTION ( 'NONE',  ( -1.000000000000000000, 0.000000000000000000, 0.000000000000000000 ) ) ;
#63318=CARTESIAN_POINT ( 'NONE',  ( 8.099999999999999645, -11.84999999999999964, 0.000000000000000000 ) ) ;
#63557=FACE_BOUND ( 'NONE', #6342, .T. ) ;
#63679=ORIENTED_EDGE ( 'NONE', *, *, #17404, .F. ) ;
#64163=( LENGTH_UNIT ( ) NAMED_UNIT ( * ) SI_UNIT ( .MILLI., .METRE. ) );
#65788=FILL_AREA_STYLE ('',( #56349 ) ) ;
#65907=CARTESIAN_POINT ( 'NONE',  ( 7.600000000000000533, 0.000000000000000000, 0.000000000000000000 ) ) ;
#65983=CIRCLE ( 'NONE', #5694, 11.84999999999999964 ) ;
#66422=ORIENTED_EDGE ( 'NONE', *, *, #45423, .T. ) ;
#66697=CARTESIAN_POINT ( 'NONE',  ( 7.100000000000000533, 0.000000000000000000, 0.000000000000000000 ) ) ;
#66816=VERTEX_POINT ( 'NONE', #63318 ) ;
#66843=PLANE ( 'NONE',  #39608 ) ;
#66904=ORIENTED_EDGE ( 'NONE', *, *, #466, .F. ) ;
#67033=AXIS2_PLACEMENT_3D ( 'NONE', #7377, #18569, #50035 ) ;
#67086=DIRECTION ( 'NONE',  ( -1.000000000000000000, 0.000000000000000000, 0.000000000000000000 ) ) ;
#68075=ORIENTED_EDGE ( 'NONE', *, *, #19973, .F. ) ;
#68179=EDGE_LOOP ( 'NONE', ( #12176, #22457, #68075, #53468 ) ) ;
#68228=CIRCLE ( 'NONE', #31421, 0.4999999999999997224 ) ;
#69151=FACE_OUTER_BOUND ( 'NONE', #60964, .T. ) ;
ENDSEC;
END-ISO-10303-21;
